ISO-10303-21;
HEADER;
FILE_DESCRIPTION (('STEP AP214'),
    '1' );
FILE_NAME ('socket head cap screw_iso_ISO 4762 M5 x 12 - 12N.step',
    '2026-10-27T08:02:39',
    ( '' ),
    ( '' ),
    'SwSTEP 2.0',
    'SolidWorks 2026',
    '' );
FILE_SCHEMA (( 'AUTOMOTIVE_DESIGN' ));
ENDSEC;

DATA;
#16=EDGE_CURVE ( 'NONE', #8654, #9068, #398, .T. ) ;
#77=FACE_BOUND ( 'NONE', #651, .T. ) ;
#94=EDGE_LOOP ( 'NONE', ( #11994, #4647, #11472, #6806 ) ) ;
#106=CARTESIAN_POINT ( 'NONE',  ( -31.74999999999995737, 5.204748896376250699E-16, -4.250000000000000000 ) ) ;
#118=CARTESIAN_POINT ( 'NONE',  ( 2.500000000000000000, -1.178949249685213863, 2.042000000000002924 ) ) ;
#129=DIRECTION ( 'NONE',  ( -1.000000000000000000, -0.000000000000000000, -0.000000000000000000 ) ) ;
#133=DIRECTION ( 'NONE',  ( -1.000000000000000000, -0.000000000000000000, -0.000000000000000000 ) ) ;
#143=UNCERTAINTY_MEASURE_WITH_UNIT (LENGTH_MEASURE( 1.000000000000000082E-05 ), #8122, 'distance_accuracy_value', 'NONE');
#147=EDGE_CURVE ( 'NONE', #5793, #9690, #7785, .T. ) ;
#163=ORIENTED_EDGE ( 'NONE', *, *, #2128, .T. ) ;
#173=CARTESIAN_POINT ( 'NONE',  ( 2.500000000000000000, -1.768423874527823791, -1.020999999999998353 ) ) ;
#198=EDGE_LOOP ( 'NONE', ( #4927, #6870, #4753, #5176, #4314 ) ) ;
#212=CARTESIAN_POINT ( 'NONE',  ( 0.000000000000000000, 0.000000000000000000, 0.000000000000000000 ) ) ;
#220=ADVANCED_FACE ( 'NONE', ( #5475 ), #2655, .F. ) ;
#247=DIRECTION ( 'NONE',  ( 0.000000000000000000, 0.000000000000000000, -1.000000000000000000 ) ) ;
#269=ORIENTED_EDGE ( 'NONE', *, *, #579, .F. ) ;
#271=ADVANCED_FACE ( 'NONE', ( #5585 ), #7380, .T. ) ;
#296=EDGE_CURVE ( 'NONE', #558, #1455, #8477, .T. ) ;
#327=ADVANCED_FACE ( 'NONE', ( #7270 ), #5314, .F. ) ;
#341=FACE_OUTER_BOUND ( 'NONE', #2342, .T. ) ;
#345=DIRECTION ( 'NONE',  ( -1.000000000000000000, -0.000000000000000000, -0.000000000000000000 ) ) ;
#374=ORIENTED_EDGE ( 'NONE', *, *, #7609, .T. ) ;
#398=LINE ( 'NONE', #8798, #3386 ) ;
#409=SURFACE_STYLE_FILL_AREA ( #4344 ) ;
#410=ORIENTED_EDGE ( 'NONE', *, *, #5322, .F. ) ;
#417=VECTOR ( 'NONE', #8737, 1000.000000000000000 ) ;
#456=FACE_OUTER_BOUND ( 'NONE', #2314, .T. ) ;
#476=DIRECTION ( 'NONE',  ( 0.000000000000000000, 0.000000000000000000, 1.000000000000000000 ) ) ;
#519=LINE ( 'NONE', #4329, #5171 ) ;
#523=UNCERTAINTY_MEASURE_WITH_UNIT (LENGTH_MEASURE( 1.000000000000000082E-05 ), #3240, 'distance_accuracy_value', 'NONE');
#527=ADVANCED_FACE ( 'NONE', ( #12108 ), #3217, .T. ) ;
#558=VERTEX_POINT ( 'NONE', #4624 ) ;
#579=EDGE_CURVE ( 'NONE', #752, #1455, #7699, .T. ) ;
#588=SHAPE_REPRESENTATION ( 'socket head cap screw_iso_ISO 4762 M5 x 12 - 12N', ( #6056 ), #8443 ) ;
#605=DIRECTION ( 'NONE',  ( 0.000000000000000000, -0.5000000000000012212, -0.8660254037844380415 ) ) ;
#606=ORIENTED_EDGE ( 'NONE', *, *, #3795, .T. ) ;
#617=AXIS2_PLACEMENT_3D ( 'NONE', #7586, #7405, #757 ) ;
#630=CARTESIAN_POINT ( 'NONE',  ( -31.74999999999995737, 0.000000000000000000, 0.000000000000000000 ) ) ;
#649=VERTEX_POINT ( 'NONE', #173 ) ;
#650=CARTESIAN_POINT ( 'NONE',  ( 0.2500000000000002220, 4.898587196589412829E-16, -4.000000000000000000 ) ) ;
#651=EDGE_LOOP ( 'NONE', ( #9311, #3965, #6290, #11424, #2951, #410 ) ) ;
#712=EDGE_CURVE ( 'NONE', #1430, #4680, #8632, .T. ) ;
#752=VERTEX_POINT ( 'NONE', #6992 ) ;
#757=DIRECTION ( 'NONE',  ( 0.000000000000000000, 0.000000000000000000, 1.000000000000000000 ) ) ;
#770=EDGE_LOOP ( 'NONE', ( #10849, #2920, #12300, #11443 ) ) ;
#778=VECTOR ( 'NONE', #11528, 1000.000000000000000 ) ;
#792=DIRECTION ( 'NONE',  ( -1.000000000000000000, -0.000000000000000000, -0.000000000000000000 ) ) ;
#793=EDGE_LOOP ( 'NONE', ( #3295, #4866 ) ) ;
#900=CARTESIAN_POINT ( 'NONE',  ( 2.500000000000000000, -1.178949249685213863, 2.042000000000002924 ) ) ;
#984=VECTOR ( 'NONE', #605, 999.9999999999998863 ) ;
#993=DIRECTION ( 'NONE',  ( 0.000000000000000000, -0.5000000000000011102, -0.8660254037844379305 ) ) ;
#1053=COLOUR_RGB ( '',1.000000000000000000, 0.9490196078431372140, 0.9098039215686274384 ) ;
#1069=VERTEX_POINT ( 'NONE', #12286 ) ;
#1074=EDGE_LOOP ( 'NONE', ( #9162, #6774, #5449, #10361 ) ) ;
#1129=DIRECTION ( 'NONE',  ( 0.000000000000000000, 0.4999999999999993894, -0.8660254037844389297 ) ) ;
#1134=DIRECTION ( 'NONE',  ( 0.000000000000000000, 1.000000000000000000, -1.471414886128461471E-15 ) ) ;
#1136=ORIENTED_EDGE ( 'NONE', *, *, #11866, .F. ) ;
#1147=LINE ( 'NONE', #6144, #1169 ) ;
#1159=LINE ( 'NONE', #11420, #417 ) ;
#1169=VECTOR ( 'NONE', #4027, 1000.000000000000000 ) ;
#1177=PLANE ( 'NONE',  #1265 ) ;
#1184=FACE_OUTER_BOUND ( 'NONE', #8896, .T. ) ;
#1219=EDGE_CURVE ( 'NONE', #649, #7970, #3167, .T. ) ;
#1225=CARTESIAN_POINT ( 'NONE',  ( 2.500000000000000000, -1.178949249685218303, -2.041999999999998039 ) ) ;
#1265=AXIS2_PLACEMENT_3D ( 'NONE', #4992, #8819, #247 ) ;
#1302=AXIS2_PLACEMENT_3D ( 'NONE', #7190, #9080, #11912 ) ;
#1310=DIRECTION ( 'NONE',  ( 0.000000000000000000, 0.000000000000000000, -1.000000000000000000 ) ) ;
#1312=DIRECTION ( 'NONE',  ( 0.000000000000000000, -1.000000000000000000, 1.287488025362403787E-15 ) ) ;
#1330=ADVANCED_FACE ( 'NONE', ( #11038, #1531 ), #4403, .T. ) ;
#1342=ORIENTED_EDGE ( 'NONE', *, *, #12054, .T. ) ;
#1351=FACE_OUTER_BOUND ( 'NONE', #198, .T. ) ;
#1389=CARTESIAN_POINT ( 'NONE',  ( 0.000000000000000000, 0.000000000000000000, 0.000000000000000000 ) ) ;
#1392=CARTESIAN_POINT ( 'NONE',  ( 2.500000000000000000, -1.178949249685213863, 2.042000000000002924 ) ) ;
#1398=AXIS2_PLACEMENT_3D ( 'NONE', #7378, #9379, #9195 ) ;
#1407=VECTOR ( 'NONE', #1312, 1000.000000000000000 ) ;
#1416=AXIS2_PLACEMENT_3D ( 'NONE', #10510, #133, #4890 ) ;
#1428=CARTESIAN_POINT ( 'NONE',  ( 0.000000000000000000, -1.178949249685213863, 2.042000000000002924 ) ) ;
#1430=VERTEX_POINT ( 'NONE', #1968 ) ;
#1433=CIRCLE ( 'NONE', #10025, 4.250000000000000000 ) ;
#1439=CARTESIAN_POINT ( 'NONE',  ( 2.500000000000000000, 0.000000000000000000, 0.000000000000000000 ) ) ;
#1442=CIRCLE ( 'NONE', #4643, 2.041999999999999815 ) ;
#1445=DIRECTION ( 'NONE',  ( 1.000000000000000000, 0.000000000000000000, 0.000000000000000000 ) ) ;
#1455=VERTEX_POINT ( 'NONE', #3909 ) ;
#1463=ORIENTED_EDGE ( 'NONE', *, *, #1219, .T. ) ;
#1467=DIRECTION ( 'NONE',  ( -1.000000000000000000, -0.000000000000000000, -0.000000000000000000 ) ) ;
#1469=ORIENTED_EDGE ( 'NONE', *, *, #1219, .F. ) ;
#1483=DIRECTION ( 'NONE',  ( -1.000000000000000000, -0.000000000000000000, -0.000000000000000000 ) ) ;
#1523=ORIENTED_EDGE ( 'NONE', *, *, #712, .T. ) ;
#1527=CARTESIAN_POINT ( 'NONE',  ( 2.500000000000000000, -2.357898499370432610, 3.252606517456513302E-15 ) ) ;
#1531=FACE_OUTER_BOUND ( 'NONE', #8588, .T. ) ;
#1558=CARTESIAN_POINT ( 'NONE',  ( 0.2500000000000002220, 5.204748896376250699E-16, -4.250000000000000000 ) ) ;
#1561=DIRECTION ( 'NONE',  ( 0.000000000000000000, -1.000000000000000000, 0.000000000000000000 ) ) ;
#1583=PLANE ( 'NONE',  #9081 ) ;
#1598=SURFACE_STYLE_USAGE ( .BOTH. , #9246 ) ;
#1670=CARTESIAN_POINT ( 'NONE',  ( 17.00000000000000000, 2.789133085058097101E-16, -2.055000000000000160 ) ) ;
#1693=CARTESIAN_POINT ( 'NONE',  ( 5.000000000000002665, 3.306546357697854226E-16, 2.700000000000000622 ) ) ;
#1716=EDGE_CURVE ( 'NONE', #11929, #9928, #1147, .T. ) ;
#1834=ADVANCED_FACE ( 'NONE', ( #4514 ), #7167, .F. ) ;
#1852=DIRECTION ( 'NONE',  ( 0.000000000000000000, 0.000000000000000000, 1.000000000000000000 ) ) ;
#1879=EDGE_CURVE ( 'NONE', #1455, #10934, #9336, .T. ) ;
#1892=CIRCLE ( 'NONE', #11854, 2.055000000000000160 ) ;
#1911=AXIS2_PLACEMENT_3D ( 'NONE', #4432, #8079, #8132 ) ;
#1966=DIRECTION ( 'NONE',  ( -1.000000000000000000, -0.000000000000000000, -0.000000000000000000 ) ) ;
#1968=CARTESIAN_POINT ( 'NONE',  ( 2.500000000000000000, -1.768423874527823569, 1.021000000000002794 ) ) ;
#1977=ADVANCED_FACE ( 'NONE', ( #3895 ), #8410, .T. ) ;
#2012=MECHANICAL_DESIGN_GEOMETRIC_PRESENTATION_REPRESENTATION('',(#3009),#5200);
#2023=EDGE_LOOP ( 'NONE', ( #10040, #3063, #10805 ) ) ;
#2026=ORIENTED_EDGE ( 'NONE', *, *, #12054, .F. ) ;
#2029=LINE ( 'NONE', #2091, #4399 ) ;
#2043=PLANE ( 'NONE',  #11253 ) ;
#2074=LINE ( 'NONE', #10747, #2096 ) ;
#2091=CARTESIAN_POINT ( 'NONE',  ( 2.500000000000000000, -2.357898499370432610, 3.252606517456513302E-15 ) ) ;
#2096=VECTOR ( 'NONE', #3191, 1000.000000000000000 ) ;
#2126=LINE ( 'NONE', #5748, #11229 ) ;
#2128=EDGE_CURVE ( 'NONE', #3878, #12234, #6840, .T. ) ;
#2149=ORIENTED_EDGE ( 'NONE', *, *, #5760, .F. ) ;
#2153=ORIENTED_EDGE ( 'NONE', *, *, #147, .F. ) ;
#2181=CARTESIAN_POINT ( 'NONE',  ( 17.00000000000000000, 0.000000000000000000, 0.000000000000000000 ) ) ;
#2199=ORIENTED_EDGE ( 'NONE', *, *, #5632, .F. ) ;
#2228=ORIENTED_EDGE ( 'NONE', *, *, #5422, .T. ) ;
#2231=ORIENTED_EDGE ( 'NONE', *, *, #9712, .T. ) ;
#2255=CARTESIAN_POINT ( 'NONE',  ( 2.500000000000000000, 2.357898499370433054, -1.951563910473907981E-15 ) ) ;
#2257=ADVANCED_FACE ( 'NONE', ( #12056 ), #9812, .F. ) ;
#2289=DIRECTION ( 'NONE',  ( -1.000000000000000000, -0.000000000000000000, -0.000000000000000000 ) ) ;
#2314=EDGE_LOOP ( 'NONE', ( #9553, #5667, #6969, #3684 ) ) ;
#2320=EDGE_CURVE ( 'NONE', #4040, #1069, #1159, .T. ) ;
#2321=ORIENTED_EDGE ( 'NONE', *, *, #16, .T. ) ;
#2342=EDGE_LOOP ( 'NONE', ( #6267, #8605, #1342, #9024, #5916 ) ) ;
#2365=PLANE ( 'NONE',  #5005 ) ;
#2389=DIRECTION ( 'NONE',  ( 0.000000000000000000, 0.000000000000000000, 1.000000000000000000 ) ) ;
#2428=AXIS2_PLACEMENT_3D ( 'NONE', #12067, #3461, #10315 ) ;
#2462=DIRECTION ( 'NONE',  ( -0.000000000000000000, 1.471414886128461471E-15, 1.000000000000000000 ) ) ;
#2478=( NAMED_UNIT ( * ) PLANE_ANGLE_UNIT ( ) SI_UNIT ( $, .RADIAN. ) );
#2495=CARTESIAN_POINT ( 'NONE',  ( 2.500000000000000000, -2.357898499370432610, 3.252606517456513302E-15 ) ) ;
#2520=DIRECTION ( 'NONE',  ( 0.000000000000000000, -1.224646799147353454E-16, 1.000000000000000000 ) ) ;
#2531=DIRECTION ( 'NONE',  ( -1.000000000000000000, -0.000000000000000000, -0.000000000000000000 ) ) ;
#2574=DIRECTION ( 'NONE',  ( 0.000000000000000000, 0.000000000000000000, -1.000000000000000000 ) ) ;
#2599=EDGE_LOOP ( 'NONE', ( #7712, #8599, #5108 ) ) ;
#2644=DIRECTION ( 'NONE',  ( -1.000000000000000000, -0.000000000000000000, -0.000000000000000000 ) ) ;
#2655=PLANE ( 'NONE',  #4379 ) ;
#2693=ORIENTED_EDGE ( 'NONE', *, *, #7950, .F. ) ;
#2731=ORIENTED_EDGE ( 'NONE', *, *, #9079, .T. ) ;
#2765=AXIS2_PLACEMENT_3D ( 'NONE', #10092, #7286, #4572 ) ;
#2818=DIRECTION ( 'NONE',  ( 1.000000000000000000, 0.000000000000000000, 0.000000000000000000 ) ) ;
#2842=AXIS2_PLACEMENT_3D ( 'NONE', #11937, #3392, #2389 ) ;
#2843=CIRCLE ( 'NONE', #6851, 2.055000000000000160 ) ;
#2848=CARTESIAN_POINT ( 'NONE',  ( 16.55500000000001393, 3.061616997868383634E-16, -2.500000000000000444 ) ) ;
#2855=ORIENTED_EDGE ( 'NONE', *, *, #296, .F. ) ;
#2863=CARTESIAN_POINT ( 'NONE',  ( 2.500000000000000000, 2.357898499370433054, -1.951563910473907981E-15 ) ) ;
#2889=EDGE_CURVE ( 'NONE', #8025, #11929, #1433, .T. ) ;
#2892=DIRECTION ( 'NONE',  ( 1.000000000000000000, 0.000000000000000000, 0.000000000000000000 ) ) ;
#2905=ORIENTED_EDGE ( 'NONE', *, *, #7613, .F. ) ;
#2917=DIRECTION ( 'NONE',  ( -1.000000000000000000, -0.000000000000000000, -0.000000000000000000 ) ) ;
#2920=ORIENTED_EDGE ( 'NONE', *, *, #2889, .T. ) ;
#2927=VERTEX_POINT ( 'NONE', #2848 ) ;
#2951=ORIENTED_EDGE ( 'NONE', *, *, #2128, .F. ) ;
#2986=( NAMED_UNIT ( * ) PLANE_ANGLE_UNIT ( ) SI_UNIT ( $, .RADIAN. ) );
#3009=STYLED_ITEM('',(#12405),#8531);
#3015=DIRECTION ( 'NONE',  ( 0.000000000000000000, 0.000000000000000000, -1.000000000000000000 ) ) ;
#3035=CIRCLE ( 'NONE', #7224, 2.700000000000000622 ) ;
#3050=AXIS2_PLACEMENT_3D ( 'NONE', #3833, #10458, #11448 ) ;
#3060=MECHANICAL_DESIGN_GEOMETRIC_PRESENTATION_REPRESENTATION('',(#7045),#5050);
#3061=CARTESIAN_POINT ( 'NONE',  ( 2.500000000000000000, 2.357898499370433054, -1.951563910473907981E-15 ) ) ;
#3063=ORIENTED_EDGE ( 'NONE', *, *, #10799, .T. ) ;
#3065=PRODUCT_CONTEXT ( 'NONE', #3872, 'mechanical' ) ;
#3070=CARTESIAN_POINT ( 'NONE',  ( 0.000000000000000000, 1.178949249685218525, 2.041999999999999371 ) ) ;
#3097=CYLINDRICAL_SURFACE ( 'NONE', #8835, 2.500000000000000444 ) ;
#3109=DIRECTION ( 'NONE',  ( 0.000000000000000000, 1.224646799147353207E-16, 1.000000000000000000 ) ) ;
#3126=CARTESIAN_POINT ( 'NONE',  ( 2.500000000000000000, 1.768423874527822681, -1.021000000000002794 ) ) ;
#3132=LINE ( 'NONE', #1428, #12137 ) ;
#3167=LINE ( 'NONE', #11773, #5201 ) ;
#3191=DIRECTION ( 'NONE',  ( 0.000000000000000000, 0.4999999999999993339, -0.8660254037844390407 ) ) ;
#3200=CARTESIAN_POINT ( 'NONE',  ( 0.000000000000000000, 1.178949249685213863, -2.042000000000001148 ) ) ;
#3217=TOROIDAL_SURFACE ( 'NONE', #1398, 4.000000000000000000, 0.2500000000000000000 ) ;
#3224=DIRECTION ( 'NONE',  ( 0.000000000000000000, 0.8660254037844380415, -0.5000000000000011102 ) ) ;
#3235=CARTESIAN_POINT ( 'NONE',  ( 2.500000000000000000, 0.000000000000000000, 0.000000000000000000 ) ) ;
#3240=( LENGTH_UNIT ( ) NAMED_UNIT ( * ) SI_UNIT ( .MILLI., .METRE. ) );
#3253=VECTOR ( 'NONE', #1483, 1000.000000000000000 ) ;
#3257=DIRECTION ( 'NONE',  ( 0.000000000000000000, -0.5000000000000011102, -0.8660254037844379305 ) ) ;
#3295=ORIENTED_EDGE ( 'NONE', *, *, #4779, .F. ) ;
#3299=AXIS2_PLACEMENT_3D ( 'NONE', #650, #10326, #2520 ) ;
#3306=ORIENTED_EDGE ( 'NONE', *, *, #4739, .T. ) ;
#3314=EDGE_LOOP ( 'NONE', ( #163, #7537, #2905, #8145, #10230 ) ) ;
#3320=ADVANCED_FACE ( 'NONE', ( #7522 ), #9238, .F. ) ;
#3356=EDGE_CURVE ( 'NONE', #8297, #5359, #10222, .T. ) ;
#3385=CARTESIAN_POINT ( 'NONE',  ( 2.500000000000000000, 2.357898499370433054, -1.951563910473907981E-15 ) ) ;
#3386=VECTOR ( 'NONE', #11710, 1000.000000000000114 ) ;
#3388=( NAMED_UNIT ( * ) SI_UNIT ( $, .STERADIAN. ) SOLID_ANGLE_UNIT ( ) );
#3392=DIRECTION ( 'NONE',  ( 1.000000000000000000, 0.000000000000000000, 0.000000000000000000 ) ) ;
#3418=PRESENTATION_STYLE_ASSIGNMENT (( #1598 ) ) ;
#3435=AXIS2_PLACEMENT_3D ( 'NONE', #630, #4512, #9391 ) ;
#3438=DIRECTION ( 'NONE',  ( 0.000000000000000000, 0.000000000000000000, 1.000000000000000000 ) ) ;
#3444=EDGE_CURVE ( 'NONE', #9643, #12234, #11814, .T. ) ;
#3461=DIRECTION ( 'NONE',  ( 1.000000000000000000, 0.000000000000000000, 0.000000000000000000 ) ) ;
#3519=PRODUCT_DEFINITION_SHAPE ( 'NONE', 'NONE',  #6878 ) ;
#3573=CARTESIAN_POINT ( 'NONE',  ( 2.500000000000000000, 1.178949249685213863, -2.042000000000001148 ) ) ;
#3592=CARTESIAN_POINT ( 'NONE',  ( 2.500000000000000000, 0.000000000000000000, 0.000000000000000000 ) ) ;
#3601=CARTESIAN_POINT ( 'NONE',  ( 0.000000000000000000, 5.051668046482832750E-16, -4.000000000000000000 ) ) ;
#3605=VERTEX_POINT ( 'NONE', #1558 ) ;
#3606=VECTOR ( 'NONE', #7815, 1000.000000000000114 ) ;
#3616=AXIS2_PLACEMENT_3D ( 'NONE', #4826, #7766, #4701 ) ;
#3619=EDGE_LOOP ( 'NONE', ( #7770, #11046, #10941, #7275 ) ) ;
#3645=DIRECTION ( 'NONE',  ( 0.000000000000000000, 0.000000000000000000, 1.000000000000000000 ) ) ;
#3659=ORIENTED_EDGE ( 'NONE', *, *, #11079, .F. ) ;
#3660=EDGE_CURVE ( 'NONE', #8639, #4145, #5055, .T. ) ;
#3681=CARTESIAN_POINT ( 'NONE',  ( 0.000000000000000000, 0.000000000000000000, 4.000000000000000000 ) ) ;
#3683=CARTESIAN_POINT ( 'NONE',  ( 2.500000000000000000, 1.178949249685218525, 2.041999999999999371 ) ) ;
#3684=ORIENTED_EDGE ( 'NONE', *, *, #6547, .T. ) ;
#3687=ORIENTED_EDGE ( 'NONE', *, *, #5099, .T. ) ;
#3734=ORIENTED_EDGE ( 'NONE', *, *, #2320, .T. ) ;
#3754=LINE ( 'NONE', #6513, #5293 ) ;
#3759=LINE ( 'NONE', #6656, #7257 ) ;
#3764=AXIS2_PLACEMENT_3D ( 'NONE', #10737, #11612, #7061 ) ;
#3795=EDGE_CURVE ( 'NONE', #752, #9690, #4811, .T. ) ;
#3817=ORIENTED_EDGE ( 'NONE', *, *, #6474, .T. ) ;
#3833=CARTESIAN_POINT ( 'NONE',  ( 5.200000000000002842, 0.000000000000000000, 0.000000000000000000 ) ) ;
#3864=CARTESIAN_POINT ( 'NONE',  ( 5.000000000000004441, 5.204748896376250699E-16, -4.250000000000000000 ) ) ;
#3872=APPLICATION_CONTEXT ( 'automotive_design' ) ;
#3876=CARTESIAN_POINT ( 'NONE',  ( 2.500000000000000000, 1.178949249685218525, 2.041999999999999371 ) ) ;
#3878=VERTEX_POINT ( 'NONE', #6066 ) ;
#3889=CARTESIAN_POINT ( 'NONE',  ( 5.000000000000004441, 0.000000000000000000, 0.000000000000000000 ) ) ;
#3892=DIRECTION ( 'NONE',  ( 0.000000000000000000, 0.000000000000000000, -1.000000000000000000 ) ) ;
#3895=FACE_OUTER_BOUND ( 'NONE', #8671, .T. ) ;
#3909=CARTESIAN_POINT ( 'NONE',  ( 2.500000000000000000, 3.004629197474318851E-15, 2.042000000000000259 ) ) ;
#3950=DIRECTION ( 'NONE',  ( 1.000000000000000000, 0.000000000000000000, 0.000000000000000000 ) ) ;
#3951=ADVANCED_FACE ( 'NONE', ( #10692 ), #1177, .F. ) ;
#3965=ORIENTED_EDGE ( 'NONE', *, *, #10059, .F. ) ;
#4027=DIRECTION ( 'NONE',  ( -1.000000000000000000, -0.000000000000000000, -0.000000000000000000 ) ) ;
#4035=DIRECTION ( 'NONE',  ( 0.000000000000000000, 0.000000000000000000, 1.000000000000000000 ) ) ;
#4040=VERTEX_POINT ( 'NONE', #11996 ) ;
#4047=DIRECTION ( 'NONE',  ( 0.000000000000000000, -0.5000000000000011102, -0.8660254037844379305 ) ) ;
#4055=EDGE_CURVE ( 'NONE', #9928, #8910, #12229, .T. ) ;
#4097=CARTESIAN_POINT ( 'NONE',  ( 2.500000000000000000, -1.178949249685213863, 2.042000000000002924 ) ) ;
#4145=VERTEX_POINT ( 'NONE', #1693 ) ;
#4229=AXIS2_PLACEMENT_3D ( 'NONE', #3235, #2289, #5157 ) ;
#4241=AXIS2_PLACEMENT_3D ( 'NONE', #7199, #10079, #9140 ) ;
#4249=PLANE ( 'NONE',  #6188 ) ;
#4277=AXIS2_PLACEMENT_3D ( 'NONE', #5960, #5908, #7023 ) ;
#4299=FACE_OUTER_BOUND ( 'NONE', #5904, .T. ) ;
#4314=ORIENTED_EDGE ( 'NONE', *, *, #7950, .T. ) ;
#4329=CARTESIAN_POINT ( 'NONE',  ( 2.500000000000000000, 1.178949249685213863, -2.042000000000001148 ) ) ;
#4333=ORIENTED_EDGE ( 'NONE', *, *, #8691, .T. ) ;
#4344=FILL_AREA_STYLE ('',( #5354 ) ) ;
#4379=AXIS2_PLACEMENT_3D ( 'NONE', #11895, #9164, #7297 ) ;
#4399=VECTOR ( 'NONE', #5912, 1000.000000000000000 ) ;
#4403=PLANE ( 'NONE',  #10608 ) ;
#4412=SHAPE_REPRESENTATION_RELATIONSHIP ( 'NONE' , 'NONE' ,  #588, #6462 ) ;
#4422=VERTEX_POINT ( 'NONE', #1670 ) ;
#4432=CARTESIAN_POINT ( 'NONE',  ( 0.000000000000000000, 0.000000000000000000, 0.000000000000000000 ) ) ;
#4457=EDGE_CURVE ( 'NONE', #1069, #2927, #10456, .T. ) ;
#4465=FACE_OUTER_BOUND ( 'NONE', #7723, .T. ) ;
#4489=EDGE_CURVE ( 'NONE', #558, #11181, #7791, .T. ) ;
#4512=DIRECTION ( 'NONE',  ( -1.000000000000000000, -0.000000000000000000, -0.000000000000000000 ) ) ;
#4514=FACE_OUTER_BOUND ( 'NONE', #11785, .T. ) ;
#4519=LINE ( 'NONE', #9157, #6973 ) ;
#4550=ADVANCED_FACE ( 'NONE', ( #8866 ), #2043, .T. ) ;
#4551=EDGE_CURVE ( 'NONE', #5359, #4145, #5676, .T. ) ;
#4572=DIRECTION ( 'NONE',  ( 0.000000000000000000, 0.000000000000000000, 1.000000000000000000 ) ) ;
#4585=CARTESIAN_POINT ( 'NONE',  ( 17.00000000000000000, 0.000000000000000000, 0.000000000000000000 ) ) ;
#4587=DIRECTION ( 'NONE',  ( 0.000000000000000000, 1.000000000000000000, -1.471414886128461471E-15 ) ) ;
#4618=CIRCLE ( 'NONE', #617, 2.041999999999999815 ) ;
#4624=CARTESIAN_POINT ( 'NONE',  ( 2.500000000000000000, -1.178949249685213863, 2.042000000000002924 ) ) ;
#4633=ADVANCED_FACE ( 'NONE', ( #10720 ), #5211, .F. ) ;
#4643=AXIS2_PLACEMENT_3D ( 'NONE', #11780, #345, #476 ) ;
#4647=ORIENTED_EDGE ( 'NONE', *, *, #11800, .T. ) ;
#4680=VERTEX_POINT ( 'NONE', #1527 ) ;
#4684=CONICAL_SURFACE ( 'NONE', #7295, 2.055000000000000160, 0.7853981633974633780 ) ;
#4696=ADVANCED_FACE ( 'NONE', ( #4465 ), #1583, .F. ) ;
#4701=DIRECTION ( 'NONE',  ( 0.000000000000000000, 0.000000000000000000, 1.000000000000000000 ) ) ;
#4709=DIRECTION ( 'NONE',  ( -1.000000000000000000, -0.000000000000000000, -0.000000000000000000 ) ) ;
#4730=EDGE_LOOP ( 'NONE', ( #11973, #10708 ) ) ;
#4739=EDGE_CURVE ( 'NONE', #3605, #12289, #11664, .T. ) ;
#4752=CARTESIAN_POINT ( 'NONE',  ( -31.74999999999995737, 0.000000000000000000, 2.500000000000000444 ) ) ;
#4753=ORIENTED_EDGE ( 'NONE', *, *, #6406, .F. ) ;
#4764=AXIS2_PLACEMENT_3D ( 'NONE', #1439, #11982, #3438 ) ;
#4779=EDGE_CURVE ( 'NONE', #4040, #4422, #1892, .T. ) ;
#4811=LINE ( 'NONE', #5558, #9259 ) ;
#4826=CARTESIAN_POINT ( 'NONE',  ( 2.500000000000000000, 0.000000000000000000, 0.000000000000000000 ) ) ;
#4851=ORIENTED_EDGE ( 'NONE', *, *, #9712, .F. ) ;
#4856=ADVANCED_FACE ( 'NONE', ( #5582 ), #4684, .T. ) ;
#4861=EDGE_LOOP ( 'NONE', ( #4851, #3306, #2199, #11836 ) ) ;
#4866=ORIENTED_EDGE ( 'NONE', *, *, #11922, .F. ) ;
#4867=AXIS2_PLACEMENT_3D ( 'NONE', #7306, #2531, #6353 ) ;
#4884=LINE ( 'NONE', #4752, #8698 ) ;
#4890=DIRECTION ( 'NONE',  ( 0.000000000000000000, 0.000000000000000000, 1.000000000000000000 ) ) ;
#4891=CARTESIAN_POINT ( 'NONE',  ( 0.2500000000000002220, 0.000000000000000000, 0.000000000000000000 ) ) ;
#4893=CARTESIAN_POINT ( 'NONE',  ( 5.200000000000002842, 0.000000000000000000, 0.000000000000000000 ) ) ;
#4927=ORIENTED_EDGE ( 'NONE', *, *, #5322, .T. ) ;
#4981=EDGE_LOOP ( 'NONE', ( #9110, #3659, #2026 ) ) ;
#4988=EDGE_CURVE ( 'NONE', #2927, #1069, #9685, .T. ) ;
#4992=CARTESIAN_POINT ( 'NONE',  ( 2.500000000000000000, 2.357898499370433054, -1.951563910473907981E-15 ) ) ;
#4998=VECTOR ( 'NONE', #5515, 999.9999999999998863 ) ;
#5005=AXIS2_PLACEMENT_3D ( 'NONE', #6192, #1445, #12227 ) ;
#5050=( GEOMETRIC_REPRESENTATION_CONTEXT ( 3 ) GLOBAL_UNCERTAINTY_ASSIGNED_CONTEXT ( ( #143 ) ) GLOBAL_UNIT_ASSIGNED_CONTEXT ( ( #8122, #2478, #7308 ) ) REPRESENTATION_CONTEXT ( 'NONE', 'WORKASPACE' ) );
#5055=CIRCLE ( 'NONE', #4241, 2.700000000000000622 ) ;
#5099=EDGE_CURVE ( 'NONE', #9690, #649, #11672, .T. ) ;
#5108=ORIENTED_EDGE ( 'NONE', *, *, #11189, .F. ) ;
#5121=CARTESIAN_POINT ( 'NONE',  ( 5.200000000000002842, 0.000000000000000000, 2.500000000000000444 ) ) ;
#5157=DIRECTION ( 'NONE',  ( 0.000000000000000000, 0.000000000000000000, 1.000000000000000000 ) ) ;
#5171=VECTOR ( 'NONE', #8157, 1000.000000000000000 ) ;
#5176=ORIENTED_EDGE ( 'NONE', *, *, #10799, .F. ) ;
#5177=DIRECTION ( 'NONE',  ( -1.000000000000000000, -0.000000000000000000, -0.000000000000000000 ) ) ;
#5185=DIRECTION ( 'NONE',  ( 1.000000000000000000, 0.000000000000000000, 0.000000000000000000 ) ) ;
#5190=VECTOR ( 'NONE', #7235, 1000.000000000000114 ) ;
#5200=( GEOMETRIC_REPRESENTATION_CONTEXT ( 3 ) GLOBAL_UNCERTAINTY_ASSIGNED_CONTEXT ( ( #5403 ) ) GLOBAL_UNIT_ASSIGNED_CONTEXT ( ( #10028, #10843, #3388 ) ) REPRESENTATION_CONTEXT ( 'NONE', 'WORKASPACE' ) );
#5201=VECTOR ( 'NONE', #9057, 1000.000000000000000 ) ;
#5208=DIRECTION ( 'NONE',  ( 0.000000000000000000, -0.4999999999999993894, 0.8660254037844389297 ) ) ;
#5211=PLANE ( 'NONE',  #7686 ) ;
#5235=VECTOR ( 'NONE', #9788, 1000.000000000000000 ) ;
#5245=AXIS2_PLACEMENT_3D ( 'NONE', #1389, #1467, #6211 ) ;
#5252=CYLINDRICAL_SURFACE ( 'NONE', #1302, 2.500000000000000444 ) ;
#5293=VECTOR ( 'NONE', #7646, 999.9999999999998863 ) ;
#5307=EDGE_CURVE ( 'NONE', #1069, #5359, #4884, .T. ) ;
#5314=PLANE ( 'NONE',  #10180 ) ;
#5322=EDGE_CURVE ( 'NONE', #10725, #3878, #3754, .T. ) ;
#5354=FILL_AREA_STYLE_COLOUR ( '', #1053 ) ;
#5359=VERTEX_POINT ( 'NONE', #5121 ) ;
#5403=UNCERTAINTY_MEASURE_WITH_UNIT (LENGTH_MEASURE( 1.000000000000000082E-05 ), #10028, 'distance_accuracy_value', 'NONE');
#5407=VECTOR ( 'NONE', #993, 1000.000000000000114 ) ;
#5411=CARTESIAN_POINT ( 'NONE',  ( 5.000000000000000888, 4.250000000000000000, 0.000000000000000000 ) ) ;
#5422=EDGE_CURVE ( 'NONE', #4680, #649, #2074, .T. ) ;
#5449=ORIENTED_EDGE ( 'NONE', *, *, #11194, .T. ) ;
#5456=DIRECTION ( 'NONE',  ( 0.000000000000000000, 0.000000000000000000, 1.000000000000000000 ) ) ;
#5459=CYLINDRICAL_SURFACE ( 'NONE', #3435, 4.250000000000000000 ) ;
#5470=CARTESIAN_POINT ( 'NONE',  ( 5.200000000000002842, 0.000000000000000000, -2.700000000000000622 ) ) ;
#5475=FACE_OUTER_BOUND ( 'NONE', #3314, .T. ) ;
#5515=DIRECTION ( 'NONE',  ( 0.000000000000000000, -0.5000000000000012212, -0.8660254037844380415 ) ) ;
#5558=CARTESIAN_POINT ( 'NONE',  ( 2.500000000000000000, 2.500728763858895382E-16, -2.041999999999999815 ) ) ;
#5582=FACE_OUTER_BOUND ( 'NONE', #8126, .T. ) ;
#5585=FACE_OUTER_BOUND ( 'NONE', #94, .T. ) ;
#5601=ORIENTED_EDGE ( 'NONE', *, *, #3356, .T. ) ;
#5632=EDGE_CURVE ( 'NONE', #8910, #12289, #7313, .T. ) ;
#5633=ADVANCED_FACE ( 'NONE', ( #4299 ), #5252, .T. ) ;
#5667=ORIENTED_EDGE ( 'NONE', *, *, #4988, .T. ) ;
#5676=CIRCLE ( 'NONE', #11060, 0.2000000000000000944 ) ;
#5682=EDGE_LOOP ( 'NONE', ( #10698, #6064, #2228, #1463, #9286 ) ) ;
#5748=CARTESIAN_POINT ( 'NONE',  ( 17.00000000000000000, 2.516649172247811061E-16, -2.055000000000000160 ) ) ;
#5760=EDGE_CURVE ( 'NONE', #10934, #7180, #8439, .T. ) ;
#5780=ORIENTED_EDGE ( 'NONE', *, *, #11800, .F. ) ;
#5783=ORIENTED_EDGE ( 'NONE', *, *, #9696, .F. ) ;
#5793=VERTEX_POINT ( 'NONE', #3126 ) ;
#5843=CIRCLE ( 'NONE', #8249, 4.250000000000000000 ) ;
#5854=CARTESIAN_POINT ( 'NONE',  ( 0.000000000000000000, -2.357898499370432610, 3.252606517456513302E-15 ) ) ;
#5861=EDGE_LOOP ( 'NONE', ( #7668, #8743, #7882, #1523, #10537 ) ) ;
#5879=ORIENTED_EDGE ( 'NONE', *, *, #5760, .T. ) ;
#5896=DIRECTION ( 'NONE',  ( 0.000000000000000000, 0.000000000000000000, -1.000000000000000000 ) ) ;
#5904=EDGE_LOOP ( 'NONE', ( #9357, #374, #5601, #10150 ) ) ;
#5908=DIRECTION ( 'NONE',  ( -1.000000000000000000, -0.000000000000000000, -0.000000000000000000 ) ) ;
#5912=DIRECTION ( 'NONE',  ( -1.000000000000000000, -0.000000000000000000, -0.000000000000000000 ) ) ;
#5916=ORIENTED_EDGE ( 'NONE', *, *, #147, .T. ) ;
#5918=CARTESIAN_POINT ( 'NONE',  ( 2.500000000000000000, -1.178949249685213863, 2.042000000000002924 ) ) ;
#5945=DIRECTION ( 'NONE',  ( -0.7071067811865369146, 8.659560562355062281E-17, -0.7071067811865582309 ) ) ;
#5959=ORIENTED_EDGE ( 'NONE', *, *, #11866, .T. ) ;
#5960=CARTESIAN_POINT ( 'NONE',  ( 16.55500000000001393, 0.000000000000000000, 0.000000000000000000 ) ) ;
#5985=CIRCLE ( 'NONE', #4764, 2.041999999999999815 ) ;
#6056=AXIS2_PLACEMENT_3D ( 'NONE', #212, #4035, #8864 ) ;
#6064=ORIENTED_EDGE ( 'NONE', *, *, #8478, .F. ) ;
#6066=CARTESIAN_POINT ( 'NONE',  ( 0.000000000000000000, 1.178949249685213863, -2.042000000000001148 ) ) ;
#6144=CARTESIAN_POINT ( 'NONE',  ( -31.74999999999995737, 0.000000000000000000, 4.250000000000000000 ) ) ;
#6150=FACE_OUTER_BOUND ( 'NONE', #8555, .T. ) ;
#6188=AXIS2_PLACEMENT_3D ( 'NONE', #11863, #8829, #1129 ) ;
#6192=CARTESIAN_POINT ( 'NONE',  ( 2.500000000000000000, 2.357898499370433054, -1.951563910473907981E-15 ) ) ;
#6210=CARTESIAN_POINT ( 'NONE',  ( 2.500000000000000000, -1.178949249685213863, 2.042000000000002924 ) ) ;
#6211=DIRECTION ( 'NONE',  ( 0.000000000000000000, 0.000000000000000000, 1.000000000000000000 ) ) ;
#6231=VECTOR ( 'NONE', #11078, 1000.000000000000000 ) ;
#6232=CARTESIAN_POINT ( 'NONE',  ( 5.000000000000000888, 0.000000000000000000, 0.000000000000000000 ) ) ;
#6248=ORIENTED_EDGE ( 'NONE', *, *, #4055, .T. ) ;
#6267=ORIENTED_EDGE ( 'NONE', *, *, #3795, .F. ) ;
#6290=ORIENTED_EDGE ( 'NONE', *, *, #10597, .T. ) ;
#6334=DIRECTION ( 'NONE',  ( 0.000000000000000000, 1.000000000000000000, -1.471414886128461471E-15 ) ) ;
#6336=ADVANCED_FACE ( 'NONE', ( #456 ), #3097, .T. ) ;
#6351=LINE ( 'NONE', #7172, #3253 ) ;
#6353=DIRECTION ( 'NONE',  ( 0.000000000000000000, 0.000000000000000000, 1.000000000000000000 ) ) ;
#6384=DIRECTION ( 'NONE',  ( -1.000000000000000000, -0.000000000000000000, -0.000000000000000000 ) ) ;
#6394=CARTESIAN_POINT ( 'NONE',  ( 5.000000000000002665, 0.000000000000000000, -2.700000000000000622 ) ) ;
#6403=CARTESIAN_POINT ( 'NONE',  ( 2.500000000000000000, 2.357898499370433054, -1.951563910473907981E-15 ) ) ;
#6406=EDGE_CURVE ( 'NONE', #5793, #10654, #9148, .T. ) ;
#6412=DIRECTION ( 'NONE',  ( 1.000000000000000000, 0.000000000000000000, 0.000000000000000000 ) ) ;
#6414=CIRCLE ( 'NONE', #3616, 2.041999999999999815 ) ;
#6424=ADVANCED_FACE ( 'NONE', ( #12002 ), #11010, .T. ) ;
#6428=AXIS2_PLACEMENT_3D ( 'NONE', #5470, #11205, #2574 ) ;
#6460=ORIENTED_EDGE ( 'NONE', *, *, #5099, .F. ) ;
#6462=ADVANCED_BREP_SHAPE_REPRESENTATION ( '', ( #8531, #6056 ), #8443 ) ;
#6469=ADVANCED_FACE ( 'NONE', ( #10088 ), #5459, .T. ) ;
#6473=DIRECTION ( 'NONE',  ( 1.000000000000000000, 0.000000000000000000, 0.000000000000000000 ) ) ;
#6474=EDGE_CURVE ( 'NONE', #10654, #9690, #8329, .T. ) ;
#6475=ORIENTED_EDGE ( 'NONE', *, *, #3660, .T. ) ;
#6513=CARTESIAN_POINT ( 'NONE',  ( 0.000000000000000000, 2.357898499370433054, -1.951563910473907981E-15 ) ) ;
#6535=ORIENTED_EDGE ( 'NONE', *, *, #11079, .T. ) ;
#6547=EDGE_CURVE ( 'NONE', #5359, #8297, #9239, .T. ) ;
#6550=ADVANCED_FACE ( 'NONE', ( #77, #11552 ), #8644, .T. ) ;
#6582=AXIS2_PLACEMENT_3D ( 'NONE', #10506, #12352, #6712 ) ;
#6586=AXIS2_PLACEMENT_3D ( 'NONE', #3592, #11953, #11212 ) ;
#6596=CARTESIAN_POINT ( 'NONE',  ( 5.000000000000004441, 0.000000000000000000, 0.000000000000000000 ) ) ;
#6625=VECTOR ( 'NONE', #4047, 1000.000000000000114 ) ;
#6627=VECTOR ( 'NONE', #5208, 1000.000000000000114 ) ;
#6631=ADVANCED_FACE ( 'NONE', ( #6650 ), #10640, .F. ) ;
#6650=FACE_OUTER_BOUND ( 'NONE', #4981, .T. ) ;
#6656=CARTESIAN_POINT ( 'NONE',  ( 0.000000000000000000, -1.178949249685213863, 2.042000000000002924 ) ) ;
#6694=EDGE_LOOP ( 'NONE', ( #6475, #7559 ) ) ;
#6712=DIRECTION ( 'NONE',  ( -0.000000000000000000, 0.000000000000000000, 1.000000000000000000 ) ) ;
#6744=LINE ( 'NONE', #10610, #6625 ) ;
#6763=ADVANCED_FACE ( 'NONE', ( #1184 ), #4249, .T. ) ;
#6774=ORIENTED_EDGE ( 'NONE', *, *, #3356, .F. ) ;
#6806=ORIENTED_EDGE ( 'NONE', *, *, #2320, .F. ) ;
#6840=LINE ( 'NONE', #3200, #1407 ) ;
#6841=ADVANCED_FACE ( 'NONE', ( #10992 ), #10125, .T. ) ;
#6851=AXIS2_PLACEMENT_3D ( 'NONE', #2181, #5177, #7001 ) ;
#6870=ORIENTED_EDGE ( 'NONE', *, *, #12044, .F. ) ;
#6878=PRODUCT_DEFINITION ( 'UNKNOWN', '', #10840, #10656 ) ;
#6895=DIRECTION ( 'NONE',  ( -1.000000000000000000, -0.000000000000000000, -0.000000000000000000 ) ) ;
#6909=VECTOR ( 'NONE', #792, 1000.000000000000000 ) ;
#6937=EDGE_CURVE ( 'NONE', #9068, #5793, #5985, .T. ) ;
#6969=ORIENTED_EDGE ( 'NONE', *, *, #5307, .T. ) ;
#6973=VECTOR ( 'NONE', #2644, 1000.000000000000000 ) ;
#6992=CARTESIAN_POINT ( 'NONE',  ( 3.678949249685231848, 0.000000000000000000, 0.000000000000000000 ) ) ;
#7001=DIRECTION ( 'NONE',  ( 0.000000000000000000, 0.000000000000000000, 1.000000000000000000 ) ) ;
#7023=DIRECTION ( 'NONE',  ( 0.000000000000000000, 0.000000000000000000, 1.000000000000000000 ) ) ;
#7026=DIRECTION ( 'NONE',  ( -1.000000000000000000, -0.000000000000000000, -0.000000000000000000 ) ) ;
#7045=STYLED_ITEM ( 'NONE', ( #3418 ), #6462 ) ;
#7061=DIRECTION ( 'NONE',  ( 0.000000000000000000, 0.5000000000000012212, 0.8660254037844380415 ) ) ;
#7104=DIRECTION ( 'NONE',  ( 0.000000000000000000, 0.000000000000000000, -1.000000000000000000 ) ) ;
#7152=ADVANCED_FACE ( 'NONE', ( #1351 ), #11540, .F. ) ;
#7154=PLANE ( 'NONE',  #9612 ) ;
#7156=DIRECTION ( 'NONE',  ( 0.000000000000000000, 0.5000000000000011102, 0.8660254037844380415 ) ) ;
#7167=CONICAL_SURFACE ( 'NONE', #2765, 2.041999999999999815, 1.047197551196591858 ) ;
#7172=CARTESIAN_POINT ( 'NONE',  ( 2.500000000000000000, 1.178949249685213863, -2.042000000000001148 ) ) ;
#7175=ORIENTED_EDGE ( 'NONE', *, *, #712, .F. ) ;
#7180=VERTEX_POINT ( 'NONE', #3070 ) ;
#7190=CARTESIAN_POINT ( 'NONE',  ( -31.74999999999995737, 0.000000000000000000, 0.000000000000000000 ) ) ;
#7199=CARTESIAN_POINT ( 'NONE',  ( 5.000000000000000888, 0.000000000000000000, 0.000000000000000000 ) ) ;
#7202=ORIENTED_EDGE ( 'NONE', *, *, #9401, .F. ) ;
#7224=AXIS2_PLACEMENT_3D ( 'NONE', #6232, #10857, #10049 ) ;
#7235=DIRECTION ( 'NONE',  ( 0.000000000000000000, -0.4999999999999993894, 0.8660254037844389297 ) ) ;
#7257=VECTOR ( 'NONE', #1134, 1000.000000000000000 ) ;
#7270=FACE_OUTER_BOUND ( 'NONE', #2023, .T. ) ;
#7275=ORIENTED_EDGE ( 'NONE', *, *, #11194, .F. ) ;
#7277=CARTESIAN_POINT ( 'NONE',  ( 0.2500000000000002220, 0.000000000000000000, 4.000000000000000000 ) ) ;
#7286=DIRECTION ( 'NONE',  ( -1.000000000000000000, -0.000000000000000000, -0.000000000000000000 ) ) ;
#7295=AXIS2_PLACEMENT_3D ( 'NONE', #7667, #4709, #11567 ) ;
#7297=DIRECTION ( 'NONE',  ( 0.000000000000000000, 1.000000000000000000, -1.287488025362403787E-15 ) ) ;
#7306=CARTESIAN_POINT ( 'NONE',  ( 16.55500000000001393, 0.000000000000000000, 0.000000000000000000 ) ) ;
#7308=( NAMED_UNIT ( * ) SI_UNIT ( $, .STERADIAN. ) SOLID_ANGLE_UNIT ( ) );
#7313=CIRCLE ( 'NONE', #1911, 4.000000000000000000 ) ;
#7339=FACE_OUTER_BOUND ( 'NONE', #10423, .T. ) ;
#7374=ORIENTED_EDGE ( 'NONE', *, *, #4739, .F. ) ;
#7378=CARTESIAN_POINT ( 'NONE',  ( 0.2500000000000002220, 0.000000000000000000, 0.000000000000000000 ) ) ;
#7380=CONICAL_SURFACE ( 'NONE', #8981, 2.055000000000000160, 0.7853981633974633780 ) ;
#7405=DIRECTION ( 'NONE',  ( -1.000000000000000000, -0.000000000000000000, -0.000000000000000000 ) ) ;
#7436=CARTESIAN_POINT ( 'NONE',  ( 0.000000000000000000, 2.357898499370433054, -1.951563910473907981E-15 ) ) ;
#7437=AXIS2_PLACEMENT_3D ( 'NONE', #12209, #6412, #9240 ) ;
#7520=ORIENTED_EDGE ( 'NONE', *, *, #8691, .F. ) ;
#7522=FACE_OUTER_BOUND ( 'NONE', #3619, .T. ) ;
#7529=ORIENTED_EDGE ( 'NONE', *, *, #7613, .T. ) ;
#7537=ORIENTED_EDGE ( 'NONE', *, *, #9529, .F. ) ;
#7559=ORIENTED_EDGE ( 'NONE', *, *, #9293, .T. ) ;
#7586=CARTESIAN_POINT ( 'NONE',  ( 2.500000000000000000, 0.000000000000000000, 0.000000000000000000 ) ) ;
#7593=CARTESIAN_POINT ( 'NONE',  ( 17.00000000000000000, 0.000000000000000000, 0.000000000000000000 ) ) ;
#7609=EDGE_CURVE ( 'NONE', #2927, #8297, #4519, .T. ) ;
#7613=EDGE_CURVE ( 'NONE', #9690, #7970, #519, .T. ) ;
#7629=CIRCLE ( 'NONE', #6428, 0.2000000000000000944 ) ;
#7646=DIRECTION ( 'NONE',  ( 0.000000000000000000, -0.5000000000000012212, -0.8660254037844380415 ) ) ;
#7667=CARTESIAN_POINT ( 'NONE',  ( 17.00000000000000000, 0.000000000000000000, 0.000000000000000000 ) ) ;
#7668=ORIENTED_EDGE ( 'NONE', *, *, #10597, .F. ) ;
#7686=AXIS2_PLACEMENT_3D ( 'NONE', #11891, #11839, #7104 ) ;
#7699=LINE ( 'NONE', #8814, #3606 ) ;
#7701=AXIS2_PLACEMENT_3D ( 'NONE', #8146, #6384, #5456 ) ;
#7712=ORIENTED_EDGE ( 'NONE', *, *, #9136, .F. ) ;
#7723=EDGE_LOOP ( 'NONE', ( #10624, #3817, #2153 ) ) ;
#7766=DIRECTION ( 'NONE',  ( -1.000000000000000000, -0.000000000000000000, -0.000000000000000000 ) ) ;
#7770=ORIENTED_EDGE ( 'NONE', *, *, #6547, .F. ) ;
#7785=CIRCLE ( 'NONE', #6586, 2.041999999999999815 ) ;
#7791=LINE ( 'NONE', #5918, #12243 ) ;
#7815=DIRECTION ( 'NONE',  ( -0.5000000000000051070, 0.000000000000000000, 0.8660254037844355990 ) ) ;
#7819=VECTOR ( 'NONE', #11598, 1000.000000000000000 ) ;
#7879=ORIENTED_EDGE ( 'NONE', *, *, #1879, .F. ) ;
#7882=ORIENTED_EDGE ( 'NONE', *, *, #9136, .T. ) ;
#7950=EDGE_CURVE ( 'NONE', #8654, #10725, #10538, .T. ) ;
#7970=VERTEX_POINT ( 'NONE', #1225 ) ;
#8025=VERTEX_POINT ( 'NONE', #3864 ) ;
#8079=DIRECTION ( 'NONE',  ( -1.000000000000000000, -0.000000000000000000, -0.000000000000000000 ) ) ;
#8091=DIRECTION ( 'NONE',  ( 0.000000000000000000, 0.4999999999999993339, -0.8660254037844390407 ) ) ;
#8101=CARTESIAN_POINT ( 'NONE',  ( -31.74999999999995737, 0.000000000000000000, 0.000000000000000000 ) ) ;
#8111=DIRECTION ( 'NONE',  ( 0.000000000000000000, 1.000000000000000000, -1.224646799147353207E-16 ) ) ;
#8122=( LENGTH_UNIT ( ) NAMED_UNIT ( * ) SI_UNIT ( .MILLI., .METRE. ) );
#8126=EDGE_LOOP ( 'NONE', ( #5780, #9941, #3734, #11249 ) ) ;
#8132=DIRECTION ( 'NONE',  ( 0.000000000000000000, 0.000000000000000000, 1.000000000000000000 ) ) ;
#8134=DIRECTION ( 'NONE',  ( -0.000000000000000000, 0.8660254037844390407, 0.4999999999999993339 ) ) ;
#8145=ORIENTED_EDGE ( 'NONE', *, *, #6474, .F. ) ;
#8146=CARTESIAN_POINT ( 'NONE',  ( 2.500000000000000000, 0.000000000000000000, 0.000000000000000000 ) ) ;
#8157=DIRECTION ( 'NONE',  ( 0.000000000000000000, -1.000000000000000000, 1.287488025362403787E-15 ) ) ;
#8165=LINE ( 'NONE', #8875, #5190 ) ;
#8175=EDGE_LOOP ( 'NONE', ( #11438, #7175, #7520 ) ) ;
#8184=CLOSED_SHELL ( 'NONE', ( #1834, #527, #3320, #8673, #5633, #271, #6550, #6424, #4856, #6336, #1330, #6469, #2257, #1977, #6763, #11076, #4550, #6841, #220, #7152, #4633, #3951, #8904, #6631, #327, #4696, #9334 ) ) ;
#8204=ORIENTED_EDGE ( 'NONE', *, *, #4489, .T. ) ;
#8239=EDGE_CURVE ( 'NONE', #10725, #7180, #8165, .T. ) ;
#8247=CIRCLE ( 'NONE', #2842, 4.250000000000000000 ) ;
#8249=AXIS2_PLACEMENT_3D ( 'NONE', #3889, #6895, #9513 ) ;
#8260=LINE ( 'NONE', #10985, #984 ) ;
#8297=VERTEX_POINT ( 'NONE', #8479 ) ;
#8329=LINE ( 'NONE', #3573, #6231 ) ;
#8397=ORIENTED_EDGE ( 'NONE', *, *, #1716, .F. ) ;
#8406=DIRECTION ( 'NONE',  ( -1.000000000000000000, -0.000000000000000000, -0.000000000000000000 ) ) ;
#8410=TOROIDAL_SURFACE ( 'NONE', #8604, 4.000000000000000000, 0.2500000000000000000 ) ;
#8439=LINE ( 'NONE', #3876, #6909 ) ;
#8443=( GEOMETRIC_REPRESENTATION_CONTEXT ( 3 ) GLOBAL_UNCERTAINTY_ASSIGNED_CONTEXT ( ( #523 ) ) GLOBAL_UNIT_ASSIGNED_CONTEXT ( ( #3240, #2986, #8742 ) ) REPRESENTATION_CONTEXT ( 'NONE', 'WORKASPACE' ) );
#8477=LINE ( 'NONE', #900, #11565 ) ;
#8478=EDGE_CURVE ( 'NONE', #4680, #9643, #2029, .T. ) ;
#8479=CARTESIAN_POINT ( 'NONE',  ( 5.200000000000002842, 3.061616997868383634E-16, -2.500000000000000444 ) ) ;
#8531=MANIFOLD_SOLID_BREP ( 'Hex', #8184 ) ;
#8555=EDGE_LOOP ( 'NONE', ( #10730, #2149, #7879, #2855, #8204 ) ) ;
#8588=EDGE_LOOP ( 'NONE', ( #1136, #12001 ) ) ;
#8599=ORIENTED_EDGE ( 'NONE', *, *, #296, .T. ) ;
#8604=AXIS2_PLACEMENT_3D ( 'NONE', #4891, #12187, #3645 ) ;
#8605=ORIENTED_EDGE ( 'NONE', *, *, #579, .T. ) ;
#8632=LINE ( 'NONE', #118, #5407 ) ;
#8635=AXIS2_PLACEMENT_3D ( 'NONE', #4893, #3950, #3015 ) ;
#8638=DIRECTION ( 'NONE',  ( -0.5000000000000051070, 1.060575238724903217E-16, -0.8660254037844355990 ) ) ;
#8639=VERTEX_POINT ( 'NONE', #6394 ) ;
#8644=PLANE ( 'NONE',  #6582 ) ;
#8654=VERTEX_POINT ( 'NONE', #9215 ) ;
#8671=EDGE_LOOP ( 'NONE', ( #7374, #7202, #6248, #5783 ) ) ;
#8673=ADVANCED_FACE ( 'NONE', ( #7339 ), #11017, .T. ) ;
#8691=EDGE_CURVE ( 'NONE', #649, #1430, #6414, .T. ) ;
#8698=VECTOR ( 'NONE', #129, 1000.000000000000000 ) ;
#8737=DIRECTION ( 'NONE',  ( -0.7071067811865369146, 0.000000000000000000, 0.7071067811865582309 ) ) ;
#8742=( NAMED_UNIT ( * ) SI_UNIT ( $, .STERADIAN. ) SOLID_ANGLE_UNIT ( ) );
#8743=ORIENTED_EDGE ( 'NONE', *, *, #4489, .F. ) ;
#8798=CARTESIAN_POINT ( 'NONE',  ( 2.500000000000000000, 2.357898499370433054, -1.951563910473907981E-15 ) ) ;
#8814=CARTESIAN_POINT ( 'NONE',  ( 2.500000000000000000, 0.000000000000000000, 2.041999999999999815 ) ) ;
#8819=DIRECTION ( 'NONE',  ( 1.000000000000000000, 0.000000000000000000, 0.000000000000000000 ) ) ;
#8829=DIRECTION ( 'NONE',  ( 0.000000000000000000, -0.8660254037844390407, -0.4999999999999994449 ) ) ;
#8832=CIRCLE ( 'NONE', #7437, 4.250000000000000000 ) ;
#8835=AXIS2_PLACEMENT_3D ( 'NONE', #8101, #7026, #11826 ) ;
#8861=CARTESIAN_POINT ( 'NONE',  ( 2.500000000000000000, -1.178949249685218303, -2.041999999999998039 ) ) ;
#8864=DIRECTION ( 'NONE',  ( 1.000000000000000000, 0.000000000000000000, 0.000000000000000000 ) ) ;
#8866=FACE_OUTER_BOUND ( 'NONE', #5861, .T. ) ;
#8875=CARTESIAN_POINT ( 'NONE',  ( 0.000000000000000000, 2.357898499370433054, -1.951563910473907981E-15 ) ) ;
#8896=EDGE_LOOP ( 'NONE', ( #11766, #2693, #2321, #6535, #5879 ) ) ;
#8904=ADVANCED_FACE ( 'NONE', ( #11869 ), #2365, .F. ) ;
#8910=VERTEX_POINT ( 'NONE', #3681 ) ;
#8974=CARTESIAN_POINT ( 'NONE',  ( 5.200000000000002842, 3.306546357697854226E-16, 2.700000000000000622 ) ) ;
#8981=AXIS2_PLACEMENT_3D ( 'NONE', #7593, #1966, #9591 ) ;
#8989=AXIS2_PLACEMENT_3D ( 'NONE', #12306, #2818, #5896 ) ;
#9017=DIRECTION ( 'NONE',  ( 1.000000000000000000, 0.000000000000000000, 0.000000000000000000 ) ) ;
#9024=ORIENTED_EDGE ( 'NONE', *, *, #6937, .T. ) ;
#9057=DIRECTION ( 'NONE',  ( 0.000000000000000000, 0.4999999999999993339, -0.8660254037844390407 ) ) ;
#9068=VERTEX_POINT ( 'NONE', #11530 ) ;
#9079=EDGE_CURVE ( 'NONE', #8025, #3605, #10677, .T. ) ;
#9080=DIRECTION ( 'NONE',  ( -1.000000000000000000, -0.000000000000000000, -0.000000000000000000 ) ) ;
#9081=AXIS2_PLACEMENT_3D ( 'NONE', #6403, #6473, #10271 ) ;
#9110=ORIENTED_EDGE ( 'NONE', *, *, #1879, .T. ) ;
#9136=EDGE_CURVE ( 'NONE', #558, #1430, #6744, .T. ) ;
#9140=DIRECTION ( 'NONE',  ( 0.000000000000000000, 0.000000000000000000, -1.000000000000000000 ) ) ;
#9148=LINE ( 'NONE', #3385, #4998 ) ;
#9157=CARTESIAN_POINT ( 'NONE',  ( -31.74999999999995737, 3.061616997868383634E-16, -2.500000000000000444 ) ) ;
#9162=ORIENTED_EDGE ( 'NONE', *, *, #4551, .F. ) ;
#9164=DIRECTION ( 'NONE',  ( 0.000000000000000000, -1.287488025362403787E-15, -1.000000000000000000 ) ) ;
#9192=DIRECTION ( 'NONE',  ( 0.000000000000000000, -0.4999999999999992784, 0.8660254037844389297 ) ) ;
#9195=DIRECTION ( 'NONE',  ( 0.000000000000000000, 0.000000000000000000, 1.000000000000000000 ) ) ;
#9215=CARTESIAN_POINT ( 'NONE',  ( 2.500000000000000000, 2.357898499370433054, -1.951563910473907981E-15 ) ) ;
#9238=TOROIDAL_SURFACE ( 'NONE', #3050, 2.700000000000000622, 0.2000000000000000111 ) ;
#9239=CIRCLE ( 'NONE', #10821, 2.500000000000000444 ) ;
#9240=DIRECTION ( 'NONE',  ( 0.000000000000000000, 0.000000000000000000, 1.000000000000000000 ) ) ;
#9246=SURFACE_SIDE_STYLE ('',( #409 ) ) ;
#9254=AXIS2_PLACEMENT_3D ( 'NONE', #2495, #8134, #9192 ) ;
#9259=VECTOR ( 'NONE', #8638, 1000.000000000000114 ) ;
#9272=DIRECTION ( 'NONE',  ( 0.000000000000000000, 0.000000000000000000, -1.000000000000000000 ) ) ;
#9286=ORIENTED_EDGE ( 'NONE', *, *, #9529, .T. ) ;
#9293=EDGE_CURVE ( 'NONE', #4145, #8639, #3035, .T. ) ;
#9311=ORIENTED_EDGE ( 'NONE', *, *, #8239, .T. ) ;
#9334=ADVANCED_FACE ( 'NONE', ( #341 ), #9437, .F. ) ;
#9336=LINE ( 'NONE', #6210, #11259 ) ;
#9348=DIRECTION ( 'NONE',  ( 0.000000000000000000, 0.000000000000000000, -1.000000000000000000 ) ) ;
#9357=ORIENTED_EDGE ( 'NONE', *, *, #4457, .T. ) ;
#9379=DIRECTION ( 'NONE',  ( -1.000000000000000000, -0.000000000000000000, -0.000000000000000000 ) ) ;
#9391=DIRECTION ( 'NONE',  ( 0.000000000000000000, 0.000000000000000000, 1.000000000000000000 ) ) ;
#9401=EDGE_CURVE ( 'NONE', #9928, #3605, #8832, .T. ) ;
#9433=DIRECTION ( 'NONE',  ( 0.000000000000000000, 0.000000000000000000, -1.000000000000000000 ) ) ;
#9437=CONICAL_SURFACE ( 'NONE', #4229, 2.041999999999999815, 1.047197551196591858 ) ;
#9446=CIRCLE ( 'NONE', #5245, 4.000000000000000000 ) ;
#9513=DIRECTION ( 'NONE',  ( 0.000000000000000000, 0.000000000000000000, 1.000000000000000000 ) ) ;
#9520=CARTESIAN_POINT ( 'NONE',  ( 0.2500000000000002220, 0.000000000000000000, 4.250000000000000000 ) ) ;
#9529=EDGE_CURVE ( 'NONE', #7970, #12234, #11517, .T. ) ;
#9553=ORIENTED_EDGE ( 'NONE', *, *, #7609, .F. ) ;
#9555=ORIENTED_EDGE ( 'NONE', *, *, #11189, .T. ) ;
#9591=DIRECTION ( 'NONE',  ( 0.000000000000000000, 0.000000000000000000, 1.000000000000000000 ) ) ;
#9612=AXIS2_PLACEMENT_3D ( 'NONE', #1392, #2462, #10099 ) ;
#9643=VERTEX_POINT ( 'NONE', #5854 ) ;
#9685=CIRCLE ( 'NONE', #4277, 2.500000000000000444 ) ;
#9690=VERTEX_POINT ( 'NONE', #10031 ) ;
#9696=EDGE_CURVE ( 'NONE', #12289, #8910, #9446, .T. ) ;
#9712=EDGE_CURVE ( 'NONE', #3605, #9928, #8247, .T. ) ;
#9788=DIRECTION ( 'NONE',  ( -1.000000000000000000, -0.000000000000000000, -0.000000000000000000 ) ) ;
#9812=TOROIDAL_SURFACE ( 'NONE', #10188, 2.700000000000000622, 0.2000000000000000111 ) ;
#9859=VECTOR ( 'NONE', #8091, 1000.000000000000000 ) ;
#9928=VERTEX_POINT ( 'NONE', #9520 ) ;
#9937=CARTESIAN_POINT ( 'NONE',  ( 2.500000000000000000, 1.178949249685213863, -2.042000000000001148 ) ) ;
#9941=ORIENTED_EDGE ( 'NONE', *, *, #11922, .T. ) ;
#10025=AXIS2_PLACEMENT_3D ( 'NONE', #6596, #10401, #1852 ) ;
#10028=( LENGTH_UNIT ( ) NAMED_UNIT ( * ) SI_UNIT ( .MILLI., .METRE. ) );
#10031=CARTESIAN_POINT ( 'NONE',  ( 2.500000000000000000, -2.629050547790028551E-15, -2.041999999999999815 ) ) ;
#10040=ORIENTED_EDGE ( 'NONE', *, *, #16, .F. ) ;
#10049=DIRECTION ( 'NONE',  ( 0.000000000000000000, 0.000000000000000000, -1.000000000000000000 ) ) ;
#10059=EDGE_CURVE ( 'NONE', #11181, #7180, #3759, .T. ) ;
#10079=DIRECTION ( 'NONE',  ( -1.000000000000000000, -0.000000000000000000, -0.000000000000000000 ) ) ;
#10085=EDGE_LOOP ( 'NONE', ( #7529, #1469, #6460 ) ) ;
#10088=FACE_OUTER_BOUND ( 'NONE', #770, .T. ) ;
#10092=CARTESIAN_POINT ( 'NONE',  ( 2.500000000000000000, 0.000000000000000000, 0.000000000000000000 ) ) ;
#10099=DIRECTION ( 'NONE',  ( 0.000000000000000000, -1.000000000000000000, 1.471414886128461471E-15 ) ) ;
#10125=PLANE ( 'NONE',  #9254 ) ;
#10150=ORIENTED_EDGE ( 'NONE', *, *, #5307, .F. ) ;
#10180=AXIS2_PLACEMENT_3D ( 'NONE', #2255, #5185, #1310 ) ;
#10188=AXIS2_PLACEMENT_3D ( 'NONE', #10421, #9017, #9433 ) ;
#10222=CIRCLE ( 'NONE', #8635, 2.500000000000000444 ) ;
#10230=ORIENTED_EDGE ( 'NONE', *, *, #12044, .T. ) ;
#10240=AXIS2_PLACEMENT_3D ( 'NONE', #7277, #1561, #9272 ) ;
#10269=CARTESIAN_POINT ( 'NONE',  ( 0.000000000000000000, -1.178949249685213863, 2.042000000000002924 ) ) ;
#10271=DIRECTION ( 'NONE',  ( 0.000000000000000000, 0.000000000000000000, -1.000000000000000000 ) ) ;
#10302=PRODUCT ( 'socket head cap screw_iso_ISO 4762 M5 x 12 - 12N', 'socket head cap screw_iso_ISO 4762 M5 x 12 - 12N', '', ( #3065 ) ) ;
#10315=DIRECTION ( 'NONE',  ( 0.000000000000000000, 0.000000000000000000, -1.000000000000000000 ) ) ;
#10326=DIRECTION ( 'NONE',  ( -0.000000000000000000, 1.000000000000000000, 1.224646799147353207E-16 ) ) ;
#10361=ORIENTED_EDGE ( 'NONE', *, *, #9293, .F. ) ;
#10401=DIRECTION ( 'NONE',  ( -1.000000000000000000, -0.000000000000000000, -0.000000000000000000 ) ) ;
#10421=CARTESIAN_POINT ( 'NONE',  ( 5.200000000000002842, 0.000000000000000000, 0.000000000000000000 ) ) ;
#10423=EDGE_LOOP ( 'NONE', ( #5959, #2731, #2231, #8397 ) ) ;
#10456=CIRCLE ( 'NONE', #4867, 2.500000000000000444 ) ;
#10458=DIRECTION ( 'NONE',  ( 1.000000000000000000, 0.000000000000000000, 0.000000000000000000 ) ) ;
#10506=CARTESIAN_POINT ( 'NONE',  ( 0.000000000000000000, 0.000000000000000000, 0.000000000000000000 ) ) ;
#10510=CARTESIAN_POINT ( 'NONE',  ( -31.74999999999995737, 0.000000000000000000, 0.000000000000000000 ) ) ;
#10537=ORIENTED_EDGE ( 'NONE', *, *, #8478, .T. ) ;
#10538=LINE ( 'NONE', #2863, #778 ) ;
#10597=EDGE_CURVE ( 'NONE', #11181, #9643, #3132, .T. ) ;
#10608=AXIS2_PLACEMENT_3D ( 'NONE', #5411, #11277, #9348 ) ;
#10610=CARTESIAN_POINT ( 'NONE',  ( 2.500000000000000000, -1.178949249685213863, 2.042000000000002924 ) ) ;
#10624=ORIENTED_EDGE ( 'NONE', *, *, #6406, .T. ) ;
#10640=PLANE ( 'NONE',  #8989 ) ;
#10654=VERTEX_POINT ( 'NONE', #9937 ) ;
#10656=PRODUCT_DEFINITION_CONTEXT ( 'detailed design', #11588, 'design' ) ;
#10677=LINE ( 'NONE', #106, #7819 ) ;
#10692=FACE_OUTER_BOUND ( 'NONE', #8175, .T. ) ;
#10698=ORIENTED_EDGE ( 'NONE', *, *, #3444, .F. ) ;
#10708=ORIENTED_EDGE ( 'NONE', *, *, #9696, .T. ) ;
#10720=FACE_OUTER_BOUND ( 'NONE', #10085, .T. ) ;
#10725=VERTEX_POINT ( 'NONE', #7436 ) ;
#10730=ORIENTED_EDGE ( 'NONE', *, *, #10059, .T. ) ;
#10737=CARTESIAN_POINT ( 'NONE',  ( 2.500000000000000000, 2.357898499370433054, -1.951563910473907981E-15 ) ) ;
#10747=CARTESIAN_POINT ( 'NONE',  ( 2.500000000000000000, -2.357898499370432610, 3.252606517456513302E-15 ) ) ;
#10799=EDGE_CURVE ( 'NONE', #8654, #5793, #8260, .T. ) ;
#10805=ORIENTED_EDGE ( 'NONE', *, *, #6937, .F. ) ;
#10810=CARTESIAN_POINT ( 'NONE',  ( 5.000000000000004441, 0.000000000000000000, 4.250000000000000000 ) ) ;
#10821=AXIS2_PLACEMENT_3D ( 'NONE', #11313, #2892, #3892 ) ;
#10840=PRODUCT_DEFINITION_FORMATION_WITH_SPECIFIED_SOURCE ( 'ANY', '', #10302, .NOT_KNOWN. ) ;
#10843=( NAMED_UNIT ( * ) PLANE_ANGLE_UNIT ( ) SI_UNIT ( $, .RADIAN. ) );
#10849=ORIENTED_EDGE ( 'NONE', *, *, #9079, .F. ) ;
#10857=DIRECTION ( 'NONE',  ( -1.000000000000000000, -0.000000000000000000, -0.000000000000000000 ) ) ;
#10934=VERTEX_POINT ( 'NONE', #3683 ) ;
#10941=ORIENTED_EDGE ( 'NONE', *, *, #3660, .F. ) ;
#10955=LINE ( 'NONE', #3061, #6627 ) ;
#10985=CARTESIAN_POINT ( 'NONE',  ( 2.500000000000000000, 2.357898499370433054, -1.951563910473907981E-15 ) ) ;
#10992=FACE_OUTER_BOUND ( 'NONE', #5682, .T. ) ;
#11010=PLANE ( 'NONE',  #2428 ) ;
#11017=CYLINDRICAL_SURFACE ( 'NONE', #1416, 4.250000000000000000 ) ;
#11038=FACE_BOUND ( 'NONE', #6694, .T. ) ;
#11046=ORIENTED_EDGE ( 'NONE', *, *, #4551, .T. ) ;
#11060=AXIS2_PLACEMENT_3D ( 'NONE', #8974, #8111, #3109 ) ;
#11076=ADVANCED_FACE ( 'NONE', ( #6150 ), #7154, .F. ) ;
#11078=DIRECTION ( 'NONE',  ( 0.000000000000000000, -1.000000000000000000, 1.287488025362403787E-15 ) ) ;
#11079=EDGE_CURVE ( 'NONE', #9068, #10934, #10955, .T. ) ;
#11181=VERTEX_POINT ( 'NONE', #10269 ) ;
#11189=EDGE_CURVE ( 'NONE', #1430, #1455, #4618, .T. ) ;
#11194=EDGE_CURVE ( 'NONE', #8297, #8639, #7629, .T. ) ;
#11205=DIRECTION ( 'NONE',  ( 0.000000000000000000, -1.000000000000000000, 0.000000000000000000 ) ) ;
#11212=DIRECTION ( 'NONE',  ( 0.000000000000000000, 0.000000000000000000, 1.000000000000000000 ) ) ;
#11229=VECTOR ( 'NONE', #5945, 1000.000000000000000 ) ;
#11249=ORIENTED_EDGE ( 'NONE', *, *, #4988, .F. ) ;
#11253=AXIS2_PLACEMENT_3D ( 'NONE', #4097, #3224, #7156 ) ;
#11259=VECTOR ( 'NONE', #6334, 1000.000000000000000 ) ;
#11277=DIRECTION ( 'NONE',  ( 1.000000000000000000, 0.000000000000000000, 0.000000000000000000 ) ) ;
#11285=SHAPE_DEFINITION_REPRESENTATION ( #3519, #588 ) ;
#11313=CARTESIAN_POINT ( 'NONE',  ( 5.200000000000002842, 0.000000000000000000, 0.000000000000000000 ) ) ;
#11333=CARTESIAN_POINT ( 'NONE',  ( 0.000000000000000000, -1.178949249685218303, -2.041999999999998039 ) ) ;
#11420=CARTESIAN_POINT ( 'NONE',  ( 17.00000000000000000, 0.000000000000000000, 2.055000000000000160 ) ) ;
#11424=ORIENTED_EDGE ( 'NONE', *, *, #3444, .T. ) ;
#11438=ORIENTED_EDGE ( 'NONE', *, *, #5422, .F. ) ;
#11443=ORIENTED_EDGE ( 'NONE', *, *, #9401, .T. ) ;
#11448=DIRECTION ( 'NONE',  ( 0.000000000000000000, 0.000000000000000000, -1.000000000000000000 ) ) ;
#11472=ORIENTED_EDGE ( 'NONE', *, *, #4457, .F. ) ;
#11517=LINE ( 'NONE', #8861, #5235 ) ;
#11528=DIRECTION ( 'NONE',  ( -1.000000000000000000, -0.000000000000000000, -0.000000000000000000 ) ) ;
#11530=CARTESIAN_POINT ( 'NONE',  ( 2.500000000000000000, 1.768423874527824902, 1.020999999999999019 ) ) ;
#11540=PLANE ( 'NONE',  #3764 ) ;
#11552=FACE_OUTER_BOUND ( 'NONE', #4730, .T. ) ;
#11565=VECTOR ( 'NONE', #4587, 1000.000000000000000 ) ;
#11567=DIRECTION ( 'NONE',  ( 0.000000000000000000, 0.000000000000000000, 1.000000000000000000 ) ) ;
#11588=APPLICATION_CONTEXT ( 'automotive_design' ) ;
#11598=DIRECTION ( 'NONE',  ( -1.000000000000000000, -0.000000000000000000, -0.000000000000000000 ) ) ;
#11612=DIRECTION ( 'NONE',  ( 0.000000000000000000, 0.8660254037844380415, -0.5000000000000012212 ) ) ;
#11664=CIRCLE ( 'NONE', #3299, 0.2500000000000002220 ) ;
#11672=CIRCLE ( 'NONE', #7701, 2.041999999999999815 ) ;
#11710=DIRECTION ( 'NONE',  ( 0.000000000000000000, -0.4999999999999993894, 0.8660254037844389297 ) ) ;
#11766=ORIENTED_EDGE ( 'NONE', *, *, #8239, .F. ) ;
#11773=CARTESIAN_POINT ( 'NONE',  ( 2.500000000000000000, -2.357898499370432610, 3.252606517456513302E-15 ) ) ;
#11780=CARTESIAN_POINT ( 'NONE',  ( 2.500000000000000000, 0.000000000000000000, 0.000000000000000000 ) ) ;
#11785=EDGE_LOOP ( 'NONE', ( #269, #606, #3687, #4333, #9555 ) ) ;
#11800=EDGE_CURVE ( 'NONE', #4422, #2927, #2126, .T. ) ;
#11814=LINE ( 'NONE', #11872, #9859 ) ;
#11826=DIRECTION ( 'NONE',  ( 0.000000000000000000, 0.000000000000000000, 1.000000000000000000 ) ) ;
#11836=ORIENTED_EDGE ( 'NONE', *, *, #4055, .F. ) ;
#11839=DIRECTION ( 'NONE',  ( 1.000000000000000000, 0.000000000000000000, 0.000000000000000000 ) ) ;
#11854=AXIS2_PLACEMENT_3D ( 'NONE', #4585, #8406, #12197 ) ;
#11863=CARTESIAN_POINT ( 'NONE',  ( 2.500000000000000000, 2.357898499370433054, -1.951563910473907981E-15 ) ) ;
#11866=EDGE_CURVE ( 'NONE', #11929, #8025, #5843, .T. ) ;
#11869=FACE_OUTER_BOUND ( 'NONE', #2599, .T. ) ;
#11872=CARTESIAN_POINT ( 'NONE',  ( 0.000000000000000000, -2.357898499370432610, 3.252606517456513302E-15 ) ) ;
#11891=CARTESIAN_POINT ( 'NONE',  ( 2.500000000000000000, 2.357898499370433054, -1.951563910473907981E-15 ) ) ;
#11895=CARTESIAN_POINT ( 'NONE',  ( 2.500000000000000000, 1.178949249685213863, -2.042000000000001148 ) ) ;
#11912=DIRECTION ( 'NONE',  ( 0.000000000000000000, 0.000000000000000000, 1.000000000000000000 ) ) ;
#11922=EDGE_CURVE ( 'NONE', #4422, #4040, #2843, .T. ) ;
#11929=VERTEX_POINT ( 'NONE', #10810 ) ;
#11937=CARTESIAN_POINT ( 'NONE',  ( 0.2500000000000002220, 0.000000000000000000, 0.000000000000000000 ) ) ;
#11953=DIRECTION ( 'NONE',  ( -1.000000000000000000, -0.000000000000000000, -0.000000000000000000 ) ) ;
#11973=ORIENTED_EDGE ( 'NONE', *, *, #5632, .T. ) ;
#11982=DIRECTION ( 'NONE',  ( -1.000000000000000000, -0.000000000000000000, -0.000000000000000000 ) ) ;
#11994=ORIENTED_EDGE ( 'NONE', *, *, #4779, .T. ) ;
#11996=CARTESIAN_POINT ( 'NONE',  ( 17.00000000000000000, 0.000000000000000000, 2.055000000000000160 ) ) ;
#12001=ORIENTED_EDGE ( 'NONE', *, *, #2889, .F. ) ;
#12002=FACE_OUTER_BOUND ( 'NONE', #793, .T. ) ;
#12044=EDGE_CURVE ( 'NONE', #10654, #3878, #6351, .T. ) ;
#12054=EDGE_CURVE ( 'NONE', #1455, #9068, #1442, .T. ) ;
#12056=FACE_OUTER_BOUND ( 'NONE', #1074, .T. ) ;
#12067=CARTESIAN_POINT ( 'NONE',  ( 17.00000000000000000, 2.055000000000000160, 0.000000000000000000 ) ) ;
#12108=FACE_OUTER_BOUND ( 'NONE', #4861, .T. ) ;
#12137=VECTOR ( 'NONE', #3257, 1000.000000000000114 ) ;
#12187=DIRECTION ( 'NONE',  ( -1.000000000000000000, -0.000000000000000000, -0.000000000000000000 ) ) ;
#12197=DIRECTION ( 'NONE',  ( 0.000000000000000000, 0.000000000000000000, 1.000000000000000000 ) ) ;
#12209=CARTESIAN_POINT ( 'NONE',  ( 0.2500000000000002220, 0.000000000000000000, 0.000000000000000000 ) ) ;
#12227=DIRECTION ( 'NONE',  ( 0.000000000000000000, 0.000000000000000000, -1.000000000000000000 ) ) ;
#12229=CIRCLE ( 'NONE', #10240, 0.2500000000000002220 ) ;
#12234=VERTEX_POINT ( 'NONE', #11333 ) ;
#12243=VECTOR ( 'NONE', #2917, 1000.000000000000000 ) ;
#12286=CARTESIAN_POINT ( 'NONE',  ( 16.55500000000001393, 0.000000000000000000, 2.500000000000000444 ) ) ;
#12289=VERTEX_POINT ( 'NONE', #3601 ) ;
#12300=ORIENTED_EDGE ( 'NONE', *, *, #1716, .T. ) ;
#12306=CARTESIAN_POINT ( 'NONE',  ( 2.500000000000000000, 2.357898499370433054, -1.951563910473907981E-15 ) ) ;
#12352=DIRECTION ( 'NONE',  ( -1.000000000000000000, 0.000000000000000000, -0.000000000000000000 ) ) ;
#12399=COLOUR_RGB('Black',0.12,0.14,0.17);
#12400=FILL_AREA_STYLE_COLOUR('',#12399);
#12401=FILL_AREA_STYLE('',(#12400));
#12402=SURFACE_STYLE_FILL_AREA(#12401);
#12403=SURFACE_SIDE_STYLE('',(#12402));
#12404=SURFACE_STYLE_USAGE(.BOTH.,#12403);
#12405=PRESENTATION_STYLE_ASSIGNMENT((#12404));
ENDSEC;
END-ISO-10303-21;
